ISO-10303-21;
HEADER;
/* Generated by software containing ST-Developer
 * from STEP Tools, Inc. (www.steptools.com) 
 */
/* OPTION: using custom renumber hook */

FILE_DESCRIPTION(
/* description */ ('STEP AP242 Edition 2', 'CAx-IF Rec.Pracs.---Representation and Presentation of Product Manufa
cturing Information (PMI)---4.0---2014-10-13', 'CAx-IF Rec.Pracs.---3D Tessellated Geometry---0.4---2014-09-14', '2;1', 'CAx-IF Rec.Pracs.---User Defined Attributes---1.5---2016-08-15'),
/* implementation_level */ '2;1');

FILE_NAME(
/* name */ 'Part 1__PD10214.step',
/* time_stamp */ '2026-10-09T13:59:33Z',
/* author */ (''),
/* organization */ (''),
/* preprocessor_version */ 'ST-DEVELOPER v20',
/* originating_system */ 'ONSHAPE BY PTC INC, 1.221',
/* authorisation */ '  ');

FILE_SCHEMA (('AP242_MANAGED_MODEL_BASED_3D_ENGINEERING_MIM_LF { 1 0 10303 442 3 1 4 }'));
ENDSEC;

DATA;
#12=CONICAL_SURFACE('',#5977,0.0025,0.785398163397445);
#20=TOROIDAL_SURFACE('',#5997,0.006,0.002);
#105=LINE('',#8882,#389);
#106=LINE('',#8885,#390);
#107=LINE('',#8887,#391);
#108=LINE('',#8889,#392);
#109=LINE('',#8891,#393);
#110=LINE('',#8894,#394);
#111=LINE('',#8896,#395);
#112=LINE('',#8898,#396);
#113=LINE('',#8900,#397);
#114=LINE('',#8902,#398);
#115=LINE('',#8905,#399);
#116=LINE('',#8909,#400);
#117=LINE('',#8913,#401);
#118=LINE('',#8915,#402);
#119=LINE('',#8918,#403);
#120=LINE('',#8920,#404);
#121=LINE('',#8922,#405);
#122=LINE('',#8924,#406);
#123=LINE('',#8926,#407);
#124=LINE('',#8929,#408);
#125=LINE('',#8931,#409);
#126=LINE('',#8933,#410);
#127=LINE('',#8935,#411);
#128=LINE('',#8938,#412);
#129=LINE('',#8940,#413);
#130=LINE('',#8942,#414);
#131=LINE('',#8944,#415);
#132=LINE('',#8946,#416);
#133=LINE('',#8949,#417);
#134=LINE('',#8951,#418);
#135=LINE('',#8953,#419);
#136=LINE('',#8955,#420);
#137=LINE('',#8958,#421);
#138=LINE('',#8960,#422);
#139=LINE('',#8962,#423);
#140=LINE('',#8964,#424);
#141=LINE('',#8969,#425);
#142=LINE('',#8999,#426);
#143=LINE('',#9006,#427);
#144=LINE('',#9009,#428);
#145=LINE('',#9019,#429);
#146=LINE('',#9024,#430);
#147=LINE('',#9026,#431);
#148=LINE('',#9042,#432);
#149=LINE('',#9046,#433);
#150=LINE('',#9048,#434);
#151=LINE('',#9052,#435);
#152=LINE('',#9054,#436);
#153=LINE('',#9058,#437);
#154=LINE('',#9060,#438);
#155=LINE('',#9062,#439);
#156=LINE('',#9065,#440);
#157=LINE('',#9069,#441);
#158=LINE('',#9071,#442);
#159=LINE('',#9073,#443);
#160=LINE('',#9077,#444);
#161=LINE('',#9079,#445);
#162=LINE('',#9084,#446);
#163=LINE('',#9086,#447);
#389=VECTOR('',#7015,1.);
#390=VECTOR('',#7016,1.);
#391=VECTOR('',#7017,1.);
#392=VECTOR('',#7018,1.);
#393=VECTOR('',#7021,1.);
#394=VECTOR('',#7022,1.);
#395=VECTOR('',#7023,1.);
#396=VECTOR('',#7024,1.);
#397=VECTOR('',#7025,1.);
#398=VECTOR('',#7028,1.);
#399=VECTOR('',#7029,1.);
#400=VECTOR('',#7032,1.);
#401=VECTOR('',#7035,1.);
#402=VECTOR('',#7038,1.);
#403=VECTOR('',#7039,1.);
#404=VECTOR('',#7040,1.);
#405=VECTOR('',#7041,1.);
#406=VECTOR('',#7042,1.);
#407=VECTOR('',#7045,1.);
#408=VECTOR('',#7046,1.);
#409=VECTOR('',#7047,1.);
#410=VECTOR('',#7048,1.);
#411=VECTOR('',#7051,1.);
#412=VECTOR('',#7052,1.);
#413=VECTOR('',#7053,1.);
#414=VECTOR('',#7054,1.);
#415=VECTOR('',#7055,1.);
#416=VECTOR('',#7058,1.);
#417=VECTOR('',#7059,1.);
#418=VECTOR('',#7060,1.);
#419=VECTOR('',#7061,1.);
#420=VECTOR('',#7064,1.);
#421=VECTOR('',#7065,1.);
#422=VECTOR('',#7066,1.);
#423=VECTOR('',#7067,1.);
#424=VECTOR('',#7068,1.);
#425=VECTOR('',#7075,1.);
#426=VECTOR('',#7110,1.);
#427=VECTOR('',#7121,1.);
#428=VECTOR('',#7124,1.);
#429=VECTOR('',#7141,1.);
#430=VECTOR('',#7144,1.);
#431=VECTOR('',#7145,1.);
#432=VECTOR('',#7168,1.);
#433=VECTOR('',#7171,1.);
#434=VECTOR('',#7174,1.);
#435=VECTOR('',#7177,1.);
#436=VECTOR('',#7178,1.);
#437=VECTOR('',#7183,1.);
#438=VECTOR('',#7186,1.);
#439=VECTOR('',#7189,1.);
#440=VECTOR('',#7192,1.);
#441=VECTOR('',#7195,1.);
#442=VECTOR('',#7196,1.);
#443=VECTOR('',#7199,1.);
#444=VECTOR('',#7202,1.);
#445=VECTOR('',#7205,1.);
#446=VECTOR('',#7212,1.);
#447=VECTOR('',#7215,1.);
#674=SHAPE_REPRESENTATION_RELATIONSHIP('','',#5692,#688);
#688=ADVANCED_BREP_SHAPE_REPRESENTATION('',(#5661),#10146);
#717=PLANE('',#5923);
#718=PLANE('',#5924);
#719=PLANE('',#5925);
#720=PLANE('',#5928);
#721=PLANE('',#5929);
#722=PLANE('',#5930);
#723=PLANE('',#5931);
#724=PLANE('',#5932);
#725=PLANE('',#5957);
#726=PLANE('',#5960);
#727=PLANE('',#5962);
#728=PLANE('',#5964);
#729=PLANE('',#5966);
#730=PLANE('',#5968);
#731=PLANE('',#5970);
#732=PLANE('',#5974);
#733=PLANE('',#5980);
#734=PLANE('',#5984);
#735=PLANE('',#5985);
#736=PLANE('',#5990);
#737=PLANE('',#5994);
#738=PLANE('',#5995);
#739=PLANE('',#6001);
#740=PLANE('',#6002);
#800=B_SPLINE_CURVE_WITH_KNOTS('',3,(#8971,#8972,#8973,#8974,#8975),
 .UNSPECIFIED.,.F.,.F.,(4,1,4),(0.,0.00143909544014382,0.00287819088028765),
 .UNSPECIFIED.);
#801=B_SPLINE_CURVE_WITH_KNOTS('',3,(#8993,#8994,#8995,#8996,#8997),
 .UNSPECIFIED.,.F.,.F.,(4,1,4),(0.,0.00143909544014381,0.00287819088028763),
 .UNSPECIFIED.);
#1232=ORIENTED_EDGE('',*,*,#2553,.T.);
#1233=ORIENTED_EDGE('',*,*,#2554,.T.);
#1234=ORIENTED_EDGE('',*,*,#2555,.T.);
#1235=ORIENTED_EDGE('',*,*,#2556,.F.);
#1236=ORIENTED_EDGE('',*,*,#2557,.T.);
#1237=ORIENTED_EDGE('',*,*,#2558,.T.);
#1238=ORIENTED_EDGE('',*,*,#2559,.T.);
#1239=ORIENTED_EDGE('',*,*,#2560,.T.);
#1240=ORIENTED_EDGE('',*,*,#2561,.T.);
#1241=ORIENTED_EDGE('',*,*,#2562,.F.);
#1242=ORIENTED_EDGE('',*,*,#2563,.T.);
#1243=ORIENTED_EDGE('',*,*,#2564,.F.);
#1244=ORIENTED_EDGE('',*,*,#2565,.F.);
#1245=ORIENTED_EDGE('',*,*,#2566,.F.);
#1246=ORIENTED_EDGE('',*,*,#2567,.T.);
#1247=ORIENTED_EDGE('',*,*,#2568,.F.);
#1248=ORIENTED_EDGE('',*,*,#2569,.T.);
#1249=ORIENTED_EDGE('',*,*,#2570,.F.);
#1250=ORIENTED_EDGE('',*,*,#2571,.F.);
#1251=ORIENTED_EDGE('',*,*,#2572,.T.);
#1252=ORIENTED_EDGE('',*,*,#2573,.F.);
#1253=ORIENTED_EDGE('',*,*,#2574,.T.);
#1254=ORIENTED_EDGE('',*,*,#2575,.T.);
#1255=ORIENTED_EDGE('',*,*,#2576,.T.);
#1256=ORIENTED_EDGE('',*,*,#2577,.F.);
#1257=ORIENTED_EDGE('',*,*,#2578,.T.);
#1258=ORIENTED_EDGE('',*,*,#2579,.F.);
#1259=ORIENTED_EDGE('',*,*,#2580,.F.);
#1260=ORIENTED_EDGE('',*,*,#2581,.T.);
#1261=ORIENTED_EDGE('',*,*,#2582,.T.);
#1262=ORIENTED_EDGE('',*,*,#2583,.T.);
#1263=ORIENTED_EDGE('',*,*,#2584,.T.);
#1264=ORIENTED_EDGE('',*,*,#2585,.F.);
#1265=ORIENTED_EDGE('',*,*,#2586,.T.);
#1266=ORIENTED_EDGE('',*,*,#2587,.T.);
#1267=ORIENTED_EDGE('',*,*,#2588,.T.);
#1268=ORIENTED_EDGE('',*,*,#2589,.T.);
#1269=ORIENTED_EDGE('',*,*,#2590,.T.);
#1270=ORIENTED_EDGE('',*,*,#2563,.F.);
#1271=ORIENTED_EDGE('',*,*,#2591,.T.);
#1272=ORIENTED_EDGE('',*,*,#2553,.F.);
#1273=ORIENTED_EDGE('',*,*,#2592,.F.);
#1274=ORIENTED_EDGE('',*,*,#2593,.F.);
#1275=ORIENTED_EDGE('',*,*,#2594,.F.);
#1276=ORIENTED_EDGE('',*,*,#2559,.F.);
#1277=ORIENTED_EDGE('',*,*,#2595,.T.);
#1278=ORIENTED_EDGE('',*,*,#2572,.F.);
#1279=ORIENTED_EDGE('',*,*,#2596,.F.);
#1280=ORIENTED_EDGE('',*,*,#2555,.F.);
#1281=ORIENTED_EDGE('',*,*,#2597,.T.);
#1282=ORIENTED_EDGE('',*,*,#2582,.F.);
#1283=ORIENTED_EDGE('',*,*,#2598,.F.);
#1284=ORIENTED_EDGE('',*,*,#2588,.F.);
#1285=ORIENTED_EDGE('',*,*,#2599,.T.);
#1286=ORIENTED_EDGE('',*,*,#2557,.F.);
#1287=ORIENTED_EDGE('',*,*,#2600,.F.);
#1288=ORIENTED_EDGE('',*,*,#2584,.F.);
#1289=ORIENTED_EDGE('',*,*,#2601,.T.);
#1290=ORIENTED_EDGE('',*,*,#2576,.F.);
#1291=ORIENTED_EDGE('',*,*,#2602,.F.);
#1292=ORIENTED_EDGE('',*,*,#2578,.F.);
#1293=ORIENTED_EDGE('',*,*,#2603,.T.);
#1294=ORIENTED_EDGE('',*,*,#2586,.F.);
#1295=ORIENTED_EDGE('',*,*,#2604,.F.);
#1296=ORIENTED_EDGE('',*,*,#2574,.F.);
#1297=ORIENTED_EDGE('',*,*,#2605,.T.);
#1298=ORIENTED_EDGE('',*,*,#2567,.F.);
#1299=ORIENTED_EDGE('',*,*,#2606,.F.);
#1300=ORIENTED_EDGE('',*,*,#2607,.F.);
#1301=ORIENTED_EDGE('',*,*,#2608,.F.);
#1302=ORIENTED_EDGE('',*,*,#2569,.F.);
#1303=ORIENTED_EDGE('',*,*,#2609,.T.);
#1304=ORIENTED_EDGE('',*,*,#2581,.F.);
#1305=ORIENTED_EDGE('',*,*,#2610,.F.);
#1306=ORIENTED_EDGE('',*,*,#2611,.T.);
#1307=ORIENTED_EDGE('',*,*,#2607,.T.);
#1308=ORIENTED_EDGE('',*,*,#2612,.F.);
#1309=ORIENTED_EDGE('',*,*,#2613,.F.);
#1310=ORIENTED_EDGE('',*,*,#2614,.F.);
#1311=ORIENTED_EDGE('',*,*,#2593,.T.);
#1312=ORIENTED_EDGE('',*,*,#2571,.T.);
#1313=ORIENTED_EDGE('',*,*,#2615,.T.);
#1314=ORIENTED_EDGE('',*,*,#2560,.F.);
#1315=ORIENTED_EDGE('',*,*,#2596,.T.);
#1316=ORIENTED_EDGE('',*,*,#2589,.F.);
#1317=ORIENTED_EDGE('',*,*,#2600,.T.);
#1318=ORIENTED_EDGE('',*,*,#2561,.F.);
#1319=ORIENTED_EDGE('',*,*,#2616,.T.);
#1320=ORIENTED_EDGE('',*,*,#2579,.T.);
#1321=ORIENTED_EDGE('',*,*,#2604,.T.);
#1322=ORIENTED_EDGE('',*,*,#2590,.F.);
#1323=ORIENTED_EDGE('',*,*,#2617,.T.);
#1324=ORIENTED_EDGE('',*,*,#2618,.T.);
#1325=ORIENTED_EDGE('',*,*,#2619,.F.);
#1326=ORIENTED_EDGE('',*,*,#2620,.F.);
#1327=ORIENTED_EDGE('',*,*,#2621,.T.);
#1328=ORIENTED_EDGE('',*,*,#2570,.T.);
#1329=ORIENTED_EDGE('',*,*,#2610,.T.);
#1330=ORIENTED_EDGE('',*,*,#2580,.T.);
#1331=ORIENTED_EDGE('',*,*,#2622,.T.);
#1332=ORIENTED_EDGE('',*,*,#2575,.F.);
#1333=ORIENTED_EDGE('',*,*,#2608,.T.);
#1334=ORIENTED_EDGE('',*,*,#2611,.F.);
#1335=ORIENTED_EDGE('',*,*,#2592,.T.);
#1336=ORIENTED_EDGE('',*,*,#2556,.T.);
#1337=ORIENTED_EDGE('',*,*,#2598,.T.);
#1338=ORIENTED_EDGE('',*,*,#2585,.T.);
#1339=ORIENTED_EDGE('',*,*,#2602,.T.);
#1340=ORIENTED_EDGE('',*,*,#2623,.T.);
#1341=ORIENTED_EDGE('',*,*,#2624,.T.);
#1342=ORIENTED_EDGE('',*,*,#2625,.F.);
#1343=ORIENTED_EDGE('',*,*,#2626,.T.);
#1344=ORIENTED_EDGE('',*,*,#2624,.F.);
#1345=ORIENTED_EDGE('',*,*,#2626,.F.);
#1346=ORIENTED_EDGE('',*,*,#2564,.T.);
#1347=ORIENTED_EDGE('',*,*,#2594,.T.);
#1348=ORIENTED_EDGE('',*,*,#2614,.T.);
#1349=ORIENTED_EDGE('',*,*,#2627,.F.);
#1350=ORIENTED_EDGE('',*,*,#2628,.F.);
#1351=ORIENTED_EDGE('',*,*,#2629,.T.);
#1352=ORIENTED_EDGE('',*,*,#2630,.F.);
#1353=ORIENTED_EDGE('',*,*,#2631,.T.);
#1354=ORIENTED_EDGE('',*,*,#2632,.F.);
#1355=ORIENTED_EDGE('',*,*,#2633,.T.);
#1356=ORIENTED_EDGE('',*,*,#2565,.T.);
#1357=ORIENTED_EDGE('',*,*,#2629,.F.);
#1358=ORIENTED_EDGE('',*,*,#2612,.T.);
#1359=ORIENTED_EDGE('',*,*,#2606,.T.);
#1360=ORIENTED_EDGE('',*,*,#2566,.T.);
#1361=ORIENTED_EDGE('',*,*,#2633,.F.);
#1362=ORIENTED_EDGE('',*,*,#2634,.F.);
#1363=ORIENTED_EDGE('',*,*,#2635,.T.);
#1364=ORIENTED_EDGE('',*,*,#2613,.T.);
#1365=ORIENTED_EDGE('',*,*,#2635,.F.);
#1366=ORIENTED_EDGE('',*,*,#2636,.F.);
#1367=ORIENTED_EDGE('',*,*,#2627,.T.);
#1368=ORIENTED_EDGE('',*,*,#2637,.F.);
#1369=ORIENTED_EDGE('',*,*,#2618,.F.);
#1370=ORIENTED_EDGE('',*,*,#2638,.F.);
#1371=ORIENTED_EDGE('',*,*,#2639,.F.);
#1372=ORIENTED_EDGE('',*,*,#2640,.F.);
#1373=ORIENTED_EDGE('',*,*,#2641,.F.);
#1374=ORIENTED_EDGE('',*,*,#2642,.F.);
#1375=ORIENTED_EDGE('',*,*,#2630,.T.);
#1376=ORIENTED_EDGE('',*,*,#2628,.T.);
#1377=ORIENTED_EDGE('',*,*,#2636,.T.);
#1378=ORIENTED_EDGE('',*,*,#2634,.T.);
#1379=ORIENTED_EDGE('',*,*,#2632,.T.);
#1380=ORIENTED_EDGE('',*,*,#2640,.T.);
#1381=ORIENTED_EDGE('',*,*,#2643,.F.);
#1382=ORIENTED_EDGE('',*,*,#2644,.F.);
#1383=ORIENTED_EDGE('',*,*,#2645,.T.);
#1384=ORIENTED_EDGE('',*,*,#2646,.F.);
#1385=ORIENTED_EDGE('',*,*,#2647,.F.);
#1386=ORIENTED_EDGE('',*,*,#2641,.T.);
#1387=ORIENTED_EDGE('',*,*,#2645,.F.);
#1388=ORIENTED_EDGE('',*,*,#2638,.T.);
#1389=ORIENTED_EDGE('',*,*,#2621,.F.);
#1390=ORIENTED_EDGE('',*,*,#2648,.F.);
#1391=ORIENTED_EDGE('',*,*,#2649,.T.);
#1392=ORIENTED_EDGE('',*,*,#2639,.T.);
#1393=ORIENTED_EDGE('',*,*,#2649,.F.);
#1394=ORIENTED_EDGE('',*,*,#2650,.F.);
#1395=ORIENTED_EDGE('',*,*,#2643,.T.);
#1396=ORIENTED_EDGE('',*,*,#2644,.T.);
#1397=ORIENTED_EDGE('',*,*,#2650,.T.);
#1398=ORIENTED_EDGE('',*,*,#2648,.T.);
#1399=ORIENTED_EDGE('',*,*,#2620,.T.);
#1400=ORIENTED_EDGE('',*,*,#2646,.T.);
#1401=ORIENTED_EDGE('',*,*,#2637,.T.);
#1402=ORIENTED_EDGE('',*,*,#2631,.F.);
#1403=ORIENTED_EDGE('',*,*,#2642,.T.);
#1404=ORIENTED_EDGE('',*,*,#2647,.T.);
#1405=ORIENTED_EDGE('',*,*,#2619,.T.);
#1406=ORIENTED_EDGE('',*,*,#2625,.T.);
#1407=ORIENTED_EDGE('',*,*,#2616,.F.);
#1408=ORIENTED_EDGE('',*,*,#2615,.F.);
#1409=ORIENTED_EDGE('',*,*,#2622,.F.);
#1410=ORIENTED_EDGE('',*,*,#2617,.F.);
#1411=ORIENTED_EDGE('',*,*,#2623,.F.);
#1412=ORIENTED_EDGE('',*,*,#2651,.T.);
#1413=ORIENTED_EDGE('',*,*,#2652,.F.);
#1414=ORIENTED_EDGE('',*,*,#2554,.F.);
#1415=ORIENTED_EDGE('',*,*,#2591,.F.);
#1416=ORIENTED_EDGE('',*,*,#2562,.T.);
#1417=ORIENTED_EDGE('',*,*,#2605,.F.);
#1418=ORIENTED_EDGE('',*,*,#2573,.T.);
#1419=ORIENTED_EDGE('',*,*,#2601,.F.);
#1420=ORIENTED_EDGE('',*,*,#2583,.F.);
#1421=ORIENTED_EDGE('',*,*,#2597,.F.);
#1422=ORIENTED_EDGE('',*,*,#2651,.F.);
#1423=ORIENTED_EDGE('',*,*,#2587,.F.);
#1424=ORIENTED_EDGE('',*,*,#2603,.F.);
#1425=ORIENTED_EDGE('',*,*,#2577,.T.);
#1426=ORIENTED_EDGE('',*,*,#2609,.F.);
#1427=ORIENTED_EDGE('',*,*,#2568,.T.);
#1428=ORIENTED_EDGE('',*,*,#2595,.F.);
#1429=ORIENTED_EDGE('',*,*,#2558,.F.);
#1430=ORIENTED_EDGE('',*,*,#2599,.F.);
#1431=ORIENTED_EDGE('',*,*,#2652,.T.);
#2553=EDGE_CURVE('',#3256,#3257,#105,.F.);
#2554=EDGE_CURVE('',#3257,#3258,#106,.T.);
#2555=EDGE_CURVE('',#3258,#3259,#107,.T.);
#2556=EDGE_CURVE('',#3256,#3259,#108,.T.);
#2557=EDGE_CURVE('',#3260,#3261,#109,.T.);
#2558=EDGE_CURVE('',#3261,#3262,#110,.T.);
#2559=EDGE_CURVE('',#3262,#3263,#111,.F.);
#2560=EDGE_CURVE('',#3263,#3264,#112,.T.);
#2561=EDGE_CURVE('',#3264,#3260,#113,.T.);
#2562=EDGE_CURVE('',#3265,#3266,#114,.T.);
#2563=EDGE_CURVE('',#3265,#3267,#115,.T.);
#2564=EDGE_CURVE('',#3268,#3267,#3779,.T.);
#2565=EDGE_CURVE('',#3269,#3268,#116,.T.);
#2566=EDGE_CURVE('',#3270,#3269,#3780,.T.);
#2567=EDGE_CURVE('',#3270,#3266,#117,.F.);
#2568=EDGE_CURVE('',#3271,#3272,#118,.T.);
#2569=EDGE_CURVE('',#3271,#3273,#119,.F.);
#2570=EDGE_CURVE('',#3274,#3273,#120,.T.);
#2571=EDGE_CURVE('',#3275,#3274,#121,.T.);
#2572=EDGE_CURVE('',#3275,#3272,#122,.T.);
#2573=EDGE_CURVE('',#3276,#3277,#123,.T.);
#2574=EDGE_CURVE('',#3276,#3278,#124,.T.);
#2575=EDGE_CURVE('',#3278,#3279,#125,.T.);
#2576=EDGE_CURVE('',#3279,#3277,#126,.F.);
#2577=EDGE_CURVE('',#3280,#3281,#127,.T.);
#2578=EDGE_CURVE('',#3280,#3282,#128,.F.);
#2579=EDGE_CURVE('',#3283,#3282,#129,.T.);
#2580=EDGE_CURVE('',#3284,#3283,#130,.T.);
#2581=EDGE_CURVE('',#3284,#3281,#131,.T.);
#2582=EDGE_CURVE('',#3285,#3286,#132,.F.);
#2583=EDGE_CURVE('',#3286,#3287,#133,.T.);
#2584=EDGE_CURVE('',#3287,#3288,#134,.T.);
#2585=EDGE_CURVE('',#3285,#3288,#135,.T.);
#2586=EDGE_CURVE('',#3289,#3290,#136,.T.);
#2587=EDGE_CURVE('',#3290,#3291,#137,.T.);
#2588=EDGE_CURVE('',#3291,#3292,#138,.F.);
#2589=EDGE_CURVE('',#3292,#3293,#139,.T.);
#2590=EDGE_CURVE('',#3293,#3289,#140,.T.);
#2591=EDGE_CURVE('',#3265,#3257,#3781,.F.);
#2592=EDGE_CURVE('',#3294,#3256,#3782,.T.);
#2593=EDGE_CURVE('',#3295,#3294,#141,.T.);
#2594=EDGE_CURVE('',#3267,#3295,#800,.T.);
#2595=EDGE_CURVE('',#3262,#3272,#3783,.F.);
#2596=EDGE_CURVE('',#3263,#3275,#3784,.F.);
#2597=EDGE_CURVE('',#3258,#3286,#3785,.F.);
#2598=EDGE_CURVE('',#3259,#3285,#3786,.T.);
#2599=EDGE_CURVE('',#3291,#3261,#3787,.F.);
#2600=EDGE_CURVE('',#3292,#3260,#3788,.F.);
#2601=EDGE_CURVE('',#3287,#3277,#3789,.F.);
#2602=EDGE_CURVE('',#3288,#3279,#3790,.T.);
#2603=EDGE_CURVE('',#3280,#3290,#3791,.F.);
#2604=EDGE_CURVE('',#3282,#3289,#3792,.F.);
#2605=EDGE_CURVE('',#3276,#3266,#3793,.F.);
#2606=EDGE_CURVE('',#3296,#3270,#801,.T.);
#2607=EDGE_CURVE('',#3297,#3296,#142,.F.);
#2608=EDGE_CURVE('',#3278,#3297,#3794,.T.);
#2609=EDGE_CURVE('',#3271,#3281,#3795,.F.);
#2610=EDGE_CURVE('',#3273,#3284,#3796,.F.);
#2611=EDGE_CURVE('',#3294,#3297,#143,.T.);
#2612=EDGE_CURVE('',#3298,#3296,#3797,.T.);
#2613=EDGE_CURVE('',#3299,#3298,#144,.T.);
#2614=EDGE_CURVE('',#3295,#3299,#3798,.T.);
#2615=EDGE_CURVE('',#3274,#3264,#3799,.T.);
#2616=EDGE_CURVE('',#3264,#3293,#3800,.T.);
#2617=EDGE_CURVE('',#3293,#3283,#3801,.T.);
#2618=EDGE_CURVE('',#3300,#3301,#145,.T.);
#2619=EDGE_CURVE('',#3302,#3301,#3802,.F.);
#2620=EDGE_CURVE('',#3303,#3302,#146,.T.);
#2621=EDGE_CURVE('',#3303,#3300,#147,.T.);
#2622=EDGE_CURVE('',#3283,#3274,#3803,.T.);
#2623=EDGE_CURVE('',#3304,#3304,#3804,.F.);
#2624=EDGE_CURVE('',#3305,#3305,#3805,.F.);
#2625=EDGE_CURVE('',#3306,#3306,#3806,.T.);
#2626=EDGE_CURVE('',#3307,#3307,#3807,.T.);
#2627=EDGE_CURVE('',#3308,#3299,#148,.T.);
#2628=EDGE_CURVE('',#3309,#3308,#3808,.T.);
#2629=EDGE_CURVE('',#3309,#3268,#149,.T.);
#2630=EDGE_CURVE('',#3310,#3309,#150,.T.);
#2631=EDGE_CURVE('',#3310,#3311,#3809,.T.);
#2632=EDGE_CURVE('',#3312,#3311,#151,.T.);
#2633=EDGE_CURVE('',#3312,#3269,#152,.T.);
#2634=EDGE_CURVE('',#3313,#3312,#3810,.T.);
#2635=EDGE_CURVE('',#3313,#3298,#153,.T.);
#2636=EDGE_CURVE('',#3308,#3313,#154,.T.);
#2637=EDGE_CURVE('',#3301,#3311,#155,.T.);
#2638=EDGE_CURVE('',#3314,#3300,#3811,.T.);
#2639=EDGE_CURVE('',#3315,#3314,#156,.T.);
#2640=EDGE_CURVE('',#3316,#3315,#3812,.T.);
#2641=EDGE_CURVE('',#3317,#3316,#157,.T.);
#2642=EDGE_CURVE('',#3310,#3317,#158,.F.);
#2643=EDGE_CURVE('',#3318,#3315,#159,.T.);
#2644=EDGE_CURVE('',#3319,#3318,#3813,.T.);
#2645=EDGE_CURVE('',#3319,#3316,#160,.T.);
#2646=EDGE_CURVE('',#3302,#3319,#161,.T.);
#2647=EDGE_CURVE('',#3317,#3302,#3814,.F.);
#2648=EDGE_CURVE('',#3320,#3303,#3815,.T.);
#2649=EDGE_CURVE('',#3320,#3314,#162,.T.);
#2650=EDGE_CURVE('',#3318,#3320,#163,.T.);
#2651=EDGE_CURVE('',#3321,#3321,#3816,.T.);
#2652=EDGE_CURVE('',#3322,#3322,#3817,.T.);
#3256=VERTEX_POINT('',#8883);
#3257=VERTEX_POINT('',#8884);
#3258=VERTEX_POINT('',#8886);
#3259=VERTEX_POINT('',#8888);
#3260=VERTEX_POINT('',#8892);
#3261=VERTEX_POINT('',#8893);
#3262=VERTEX_POINT('',#8895);
#3263=VERTEX_POINT('',#8897);
#3264=VERTEX_POINT('',#8899);
#3265=VERTEX_POINT('',#8903);
#3266=VERTEX_POINT('',#8904);
#3267=VERTEX_POINT('',#8906);
#3268=VERTEX_POINT('',#8908);
#3269=VERTEX_POINT('',#8910);
#3270=VERTEX_POINT('',#8912);
#3271=VERTEX_POINT('',#8916);
#3272=VERTEX_POINT('',#8917);
#3273=VERTEX_POINT('',#8919);
#3274=VERTEX_POINT('',#8921);
#3275=VERTEX_POINT('',#8923);
#3276=VERTEX_POINT('',#8927);
#3277=VERTEX_POINT('',#8928);
#3278=VERTEX_POINT('',#8930);
#3279=VERTEX_POINT('',#8932);
#3280=VERTEX_POINT('',#8936);
#3281=VERTEX_POINT('',#8937);
#3282=VERTEX_POINT('',#8939);
#3283=VERTEX_POINT('',#8941);
#3284=VERTEX_POINT('',#8943);
#3285=VERTEX_POINT('',#8947);
#3286=VERTEX_POINT('',#8948);
#3287=VERTEX_POINT('',#8950);
#3288=VERTEX_POINT('',#8952);
#3289=VERTEX_POINT('',#8956);
#3290=VERTEX_POINT('',#8957);
#3291=VERTEX_POINT('',#8959);
#3292=VERTEX_POINT('',#8961);
#3293=VERTEX_POINT('',#8963);
#3294=VERTEX_POINT('',#8968);
#3295=VERTEX_POINT('',#8970);
#3296=VERTEX_POINT('',#8998);
#3297=VERTEX_POINT('',#9000);
#3298=VERTEX_POINT('',#9008);
#3299=VERTEX_POINT('',#9010);
#3300=VERTEX_POINT('',#9020);
#3301=VERTEX_POINT('',#9021);
#3302=VERTEX_POINT('',#9023);
#3303=VERTEX_POINT('',#9025);
#3304=VERTEX_POINT('',#9032);
#3305=VERTEX_POINT('',#9034);
#3306=VERTEX_POINT('',#9037);
#3307=VERTEX_POINT('',#9039);
#3308=VERTEX_POINT('',#9043);
#3309=VERTEX_POINT('',#9045);
#3310=VERTEX_POINT('',#9049);
#3311=VERTEX_POINT('',#9051);
#3312=VERTEX_POINT('',#9053);
#3313=VERTEX_POINT('',#9057);
#3314=VERTEX_POINT('',#9064);
#3315=VERTEX_POINT('',#9066);
#3316=VERTEX_POINT('',#9068);
#3317=VERTEX_POINT('',#9070);
#3318=VERTEX_POINT('',#9074);
#3319=VERTEX_POINT('',#9076);
#3320=VERTEX_POINT('',#9083);
#3321=VERTEX_POINT('',#9092);
#3322=VERTEX_POINT('',#9094);
#3779=CIRCLE('',#5926,0.002);
#3780=CIRCLE('',#5927,0.002);
#3781=CIRCLE('',#5934,0.002);
#3782=CIRCLE('',#5935,0.002);
#3783=CIRCLE('',#5937,0.002);
#3784=CIRCLE('',#5938,0.002);
#3785=CIRCLE('',#5940,0.002);
#3786=CIRCLE('',#5941,0.002);
#3787=CIRCLE('',#5943,0.002);
#3788=CIRCLE('',#5944,0.002);
#3789=CIRCLE('',#5946,0.002);
#3790=CIRCLE('',#5947,0.002);
#3791=CIRCLE('',#5949,0.002);
#3792=CIRCLE('',#5950,0.002);
#3793=CIRCLE('',#5952,0.002);
#3794=CIRCLE('',#5953,0.002);
#3795=CIRCLE('',#5955,0.002);
#3796=CIRCLE('',#5956,0.002);
#3797=CIRCLE('',#5958,0.002);
#3798=CIRCLE('',#5959,0.002);
#3799=CIRCLE('',#5961,0.006);
#3800=CIRCLE('',#5963,0.006);
#3801=CIRCLE('',#5965,0.006);
#3802=CIRCLE('',#5967,0.0015);
#3803=CIRCLE('',#5969,0.006);
#3804=CIRCLE('',#5972,0.004);
#3805=CIRCLE('',#5973,0.004);
#3806=CIRCLE('',#5975,0.0015);
#3807=CIRCLE('',#5976,0.0025);
#3808=CIRCLE('',#5979,0.002);
#3809=CIRCLE('',#5981,0.0015);
#3810=CIRCLE('',#5983,0.002);
#3811=CIRCLE('',#5986,0.0015);
#3812=CIRCLE('',#5987,0.0015);
#3813=CIRCLE('',#5989,0.0015);
#3814=CIRCLE('',#5991,0.0015);
#3815=CIRCLE('',#5993,0.0015);
#3816=CIRCLE('',#5999,0.00500637669063053);
#3817=CIRCLE('',#6000,0.00500637669063053);
#4221=EDGE_LOOP('',(#1232,#1233,#1234,#1235));
#4222=EDGE_LOOP('',(#1236,#1237,#1238,#1239,#1240));
#4223=EDGE_LOOP('',(#1241,#1242,#1243,#1244,#1245,#1246));
#4224=EDGE_LOOP('',(#1247,#1248,#1249,#1250,#1251));
#4225=EDGE_LOOP('',(#1252,#1253,#1254,#1255));
#4226=EDGE_LOOP('',(#1256,#1257,#1258,#1259,#1260));
#4227=EDGE_LOOP('',(#1261,#1262,#1263,#1264));
#4228=EDGE_LOOP('',(#1265,#1266,#1267,#1268,#1269));
#4229=EDGE_LOOP('',(#1270,#1271,#1272,#1273,#1274,#1275));
#4230=EDGE_LOOP('',(#1276,#1277,#1278,#1279));
#4231=EDGE_LOOP('',(#1280,#1281,#1282,#1283));
#4232=EDGE_LOOP('',(#1284,#1285,#1286,#1287));
#4233=EDGE_LOOP('',(#1288,#1289,#1290,#1291));
#4234=EDGE_LOOP('',(#1292,#1293,#1294,#1295));
#4235=EDGE_LOOP('',(#1296,#1297,#1298,#1299,#1300,#1301));
#4236=EDGE_LOOP('',(#1302,#1303,#1304,#1305));
#4237=EDGE_LOOP('',(#1306,#1307,#1308,#1309,#1310,#1311));
#4238=EDGE_LOOP('',(#1312,#1313,#1314,#1315));
#4239=EDGE_LOOP('',(#1316,#1317,#1318,#1319));
#4240=EDGE_LOOP('',(#1320,#1321,#1322,#1323));
#4241=EDGE_LOOP('',(#1324,#1325,#1326,#1327));
#4242=EDGE_LOOP('',(#1328,#1329,#1330,#1331));
#4243=EDGE_LOOP('',(#1332,#1333,#1334,#1335,#1336,#1337,#1338,#1339));
#4244=EDGE_LOOP('',(#1340));
#4245=EDGE_LOOP('',(#1341));
#4246=EDGE_LOOP('',(#1342));
#4247=EDGE_LOOP('',(#1343));
#4248=EDGE_LOOP('',(#1344));
#4249=EDGE_LOOP('',(#1345));
#4250=EDGE_LOOP('',(#1346,#1347,#1348,#1349,#1350,#1351));
#4251=EDGE_LOOP('',(#1352,#1353,#1354,#1355,#1356,#1357));
#4252=EDGE_LOOP('',(#1358,#1359,#1360,#1361,#1362,#1363));
#4253=EDGE_LOOP('',(#1364,#1365,#1366,#1367));
#4254=EDGE_LOOP('',(#1368,#1369,#1370,#1371,#1372,#1373,#1374,#1375,#1376,
#1377,#1378,#1379));
#4255=EDGE_LOOP('',(#1380,#1381,#1382,#1383));
#4256=EDGE_LOOP('',(#1384,#1385,#1386,#1387));
#4257=EDGE_LOOP('',(#1388,#1389,#1390,#1391));
#4258=EDGE_LOOP('',(#1392,#1393,#1394,#1395));
#4259=EDGE_LOOP('',(#1396,#1397,#1398,#1399,#1400));
#4260=EDGE_LOOP('',(#1401,#1402,#1403,#1404,#1405));
#4261=EDGE_LOOP('',(#1406));
#4262=EDGE_LOOP('',(#1407,#1408,#1409,#1410));
#4263=EDGE_LOOP('',(#1411));
#4264=EDGE_LOOP('',(#1412));
#4265=EDGE_LOOP('',(#1413));
#4266=EDGE_LOOP('',(#1414,#1415,#1416,#1417,#1418,#1419,#1420,#1421));
#4267=EDGE_LOOP('',(#1422));
#4268=EDGE_LOOP('',(#1423,#1424,#1425,#1426,#1427,#1428,#1429,#1430));
#4269=EDGE_LOOP('',(#1431));
#4669=FACE_BOUND('',#4221,.T.);
#4670=FACE_BOUND('',#4222,.T.);
#4671=FACE_BOUND('',#4223,.T.);
#4672=FACE_BOUND('',#4224,.T.);
#4673=FACE_BOUND('',#4225,.T.);
#4674=FACE_BOUND('',#4226,.T.);
#4675=FACE_BOUND('',#4227,.T.);
#4676=FACE_BOUND('',#4228,.T.);
#4677=FACE_BOUND('',#4229,.T.);
#4678=FACE_BOUND('',#4230,.T.);
#4679=FACE_BOUND('',#4231,.T.);
#4680=FACE_BOUND('',#4232,.T.);
#4681=FACE_BOUND('',#4233,.T.);
#4682=FACE_BOUND('',#4234,.T.);
#4683=FACE_BOUND('',#4235,.T.);
#4684=FACE_BOUND('',#4236,.T.);
#4685=FACE_BOUND('',#4237,.T.);
#4686=FACE_BOUND('',#4238,.T.);
#4687=FACE_BOUND('',#4239,.T.);
#4688=FACE_BOUND('',#4240,.T.);
#4689=FACE_BOUND('',#4241,.T.);
#4690=FACE_BOUND('',#4242,.T.);
#4691=FACE_BOUND('',#4243,.T.);
#4692=FACE_BOUND('',#4244,.T.);
#4693=FACE_BOUND('',#4245,.T.);
#4694=FACE_BOUND('',#4246,.T.);
#4695=FACE_BOUND('',#4247,.T.);
#4696=FACE_BOUND('',#4248,.T.);
#4697=FACE_BOUND('',#4249,.T.);
#4698=FACE_BOUND('',#4250,.T.);
#4699=FACE_BOUND('',#4251,.T.);
#4700=FACE_BOUND('',#4252,.T.);
#4701=FACE_BOUND('',#4253,.T.);
#4702=FACE_BOUND('',#4254,.T.);
#4703=FACE_BOUND('',#4255,.T.);
#4704=FACE_BOUND('',#4256,.T.);
#4705=FACE_BOUND('',#4257,.T.);
#4706=FACE_BOUND('',#4258,.T.);
#4707=FACE_BOUND('',#4259,.T.);
#4708=FACE_BOUND('',#4260,.T.);
#4709=FACE_BOUND('',#4261,.T.);
#4710=FACE_BOUND('',#4262,.T.);
#4711=FACE_BOUND('',#4263,.T.);
#4712=FACE_BOUND('',#4264,.T.);
#4713=FACE_BOUND('',#4265,.T.);
#4714=FACE_BOUND('',#4266,.T.);
#4715=FACE_BOUND('',#4267,.T.);
#4716=FACE_BOUND('',#4268,.T.);
#4717=FACE_BOUND('',#4269,.T.);
#5064=CYLINDRICAL_SURFACE('',#5933,0.002);
#5065=CYLINDRICAL_SURFACE('',#5936,0.002);
#5066=CYLINDRICAL_SURFACE('',#5939,0.002);
#5067=CYLINDRICAL_SURFACE('',#5942,0.002);
#5068=CYLINDRICAL_SURFACE('',#5945,0.002);
#5069=CYLINDRICAL_SURFACE('',#5948,0.002);
#5070=CYLINDRICAL_SURFACE('',#5951,0.002);
#5071=CYLINDRICAL_SURFACE('',#5954,0.002);
#5072=CYLINDRICAL_SURFACE('',#5971,0.004);
#5073=CYLINDRICAL_SURFACE('',#5978,0.002);
#5074=CYLINDRICAL_SURFACE('',#5982,0.002);
#5075=CYLINDRICAL_SURFACE('',#5988,0.0015);
#5076=CYLINDRICAL_SURFACE('',#5992,0.0015);
#5077=CYLINDRICAL_SURFACE('',#5996,0.0015);
#5078=CYLINDRICAL_SURFACE('',#5998,0.00500637669063053);
#5297=ADVANCED_FACE('',(#4669),#717,.T.);
#5298=ADVANCED_FACE('',(#4670),#718,.T.);
#5299=ADVANCED_FACE('',(#4671),#719,.F.);
#5300=ADVANCED_FACE('',(#4672),#720,.F.);
#5301=ADVANCED_FACE('',(#4673),#721,.F.);
#5302=ADVANCED_FACE('',(#4674),#722,.F.);
#5303=ADVANCED_FACE('',(#4675),#723,.T.);
#5304=ADVANCED_FACE('',(#4676),#724,.T.);
#5305=ADVANCED_FACE('',(#4677),#5064,.T.);
#5306=ADVANCED_FACE('',(#4678),#5065,.T.);
#5307=ADVANCED_FACE('',(#4679),#5066,.T.);
#5308=ADVANCED_FACE('',(#4680),#5067,.T.);
#5309=ADVANCED_FACE('',(#4681),#5068,.T.);
#5310=ADVANCED_FACE('',(#4682),#5069,.T.);
#5311=ADVANCED_FACE('',(#4683),#5070,.T.);
#5312=ADVANCED_FACE('',(#4684),#5071,.T.);
#5313=ADVANCED_FACE('',(#4685),#725,.F.);
#5314=ADVANCED_FACE('',(#4686),#726,.F.);
#5315=ADVANCED_FACE('',(#4687),#727,.F.);
#5316=ADVANCED_FACE('',(#4688),#728,.F.);
#5317=ADVANCED_FACE('',(#4689),#729,.F.);
#5318=ADVANCED_FACE('',(#4690),#730,.F.);
#5319=ADVANCED_FACE('',(#4691),#731,.T.);
#5320=ADVANCED_FACE('',(#4692,#4693),#5072,.T.);
#5321=ADVANCED_FACE('',(#4694,#4695),#732,.T.);
#5322=ADVANCED_FACE('',(#4696,#4697),#12,.T.);
#5323=ADVANCED_FACE('',(#4698),#5073,.F.);
#5324=ADVANCED_FACE('',(#4699),#733,.F.);
#5325=ADVANCED_FACE('',(#4700),#5074,.F.);
#5326=ADVANCED_FACE('',(#4701),#734,.F.);
#5327=ADVANCED_FACE('',(#4702),#735,.T.);
#5328=ADVANCED_FACE('',(#4703),#5075,.F.);
#5329=ADVANCED_FACE('',(#4704),#736,.F.);
#5330=ADVANCED_FACE('',(#4705),#5076,.F.);
#5331=ADVANCED_FACE('',(#4706),#737,.F.);
#5332=ADVANCED_FACE('',(#4707),#738,.T.);
#5333=ADVANCED_FACE('',(#4708,#4709),#5077,.F.);
#5334=ADVANCED_FACE('',(#4710,#4711),#20,.F.);
#5335=ADVANCED_FACE('',(#4712,#4713),#5078,.T.);
#5336=ADVANCED_FACE('',(#4714,#4715),#739,.T.);
#5337=ADVANCED_FACE('',(#4716,#4717),#740,.T.);
#5542=CLOSED_SHELL('',(#5297,#5298,#5299,#5300,#5301,#5302,#5303,#5304,
#5305,#5306,#5307,#5308,#5309,#5310,#5311,#5312,#5313,#5314,#5315,#5316,
#5317,#5318,#5319,#5320,#5321,#5322,#5323,#5324,#5325,#5326,#5327,#5328,
#5329,#5330,#5331,#5332,#5333,#5334,#5335,#5336,#5337));
#5556=STYLED_ITEM('',(#5570),#5661);
#5570=PRESENTATION_STYLE_ASSIGNMENT((#5584));
#5584=SURFACE_STYLE_USAGE(.BOTH.,#5598);
#5598=SURFACE_SIDE_STYLE('',(#5612));
#5612=SURFACE_STYLE_FILL_AREA(#5626);
#5626=FILL_AREA_STYLE('',(#5640));
#5640=FILL_AREA_STYLE_COLOUR('',#5654);
#5654=COLOUR_RGB('', 0.72549020, 0.75294118, 0.79215686);
#5661=MANIFOLD_SOLID_BREP('Part 1',#5542);
#5676=SHAPE_DEFINITION_REPRESENTATION(#10186,#5692);
#5692=SHAPE_REPRESENTATION('Part 1',(#5704),#10146);
#5704=AXIS2_PLACEMENT_3D('',#8391,#6505,#6506);
#5923=AXIS2_PLACEMENT_3D('',#8881,#7013,#7014);
#5924=AXIS2_PLACEMENT_3D('',#8890,#7019,#7020);
#5925=AXIS2_PLACEMENT_3D('',#8901,#7026,#7027);
#5926=AXIS2_PLACEMENT_3D('',#8907,#7030,#7031);
#5927=AXIS2_PLACEMENT_3D('',#8911,#7033,#7034);
#5928=AXIS2_PLACEMENT_3D('',#8914,#7036,#7037);
#5929=AXIS2_PLACEMENT_3D('',#8925,#7043,#7044);
#5930=AXIS2_PLACEMENT_3D('',#8934,#7049,#7050);
#5931=AXIS2_PLACEMENT_3D('',#8945,#7056,#7057);
#5932=AXIS2_PLACEMENT_3D('',#8954,#7062,#7063);
#5933=AXIS2_PLACEMENT_3D('',#8965,#7069,#7070);
#5934=AXIS2_PLACEMENT_3D('',#8966,#7071,#7072);
#5935=AXIS2_PLACEMENT_3D('',#8967,#7073,#7074);
#5936=AXIS2_PLACEMENT_3D('',#8976,#7076,#7077);
#5937=AXIS2_PLACEMENT_3D('',#8977,#7078,#7079);
#5938=AXIS2_PLACEMENT_3D('',#8978,#7080,#7081);
#5939=AXIS2_PLACEMENT_3D('',#8979,#7082,#7083);
#5940=AXIS2_PLACEMENT_3D('',#8980,#7084,#7085);
#5941=AXIS2_PLACEMENT_3D('',#8981,#7086,#7087);
#5942=AXIS2_PLACEMENT_3D('',#8982,#7088,#7089);
#5943=AXIS2_PLACEMENT_3D('',#8983,#7090,#7091);
#5944=AXIS2_PLACEMENT_3D('',#8984,#7092,#7093);
#5945=AXIS2_PLACEMENT_3D('',#8985,#7094,#7095);
#5946=AXIS2_PLACEMENT_3D('',#8986,#7096,#7097);
#5947=AXIS2_PLACEMENT_3D('',#8987,#7098,#7099);
#5948=AXIS2_PLACEMENT_3D('',#8988,#7100,#7101);
#5949=AXIS2_PLACEMENT_3D('',#8989,#7102,#7103);
#5950=AXIS2_PLACEMENT_3D('',#8990,#7104,#7105);
#5951=AXIS2_PLACEMENT_3D('',#8991,#7106,#7107);
#5952=AXIS2_PLACEMENT_3D('',#8992,#7108,#7109);
#5953=AXIS2_PLACEMENT_3D('',#9001,#7111,#7112);
#5954=AXIS2_PLACEMENT_3D('',#9002,#7113,#7114);
#5955=AXIS2_PLACEMENT_3D('',#9003,#7115,#7116);
#5956=AXIS2_PLACEMENT_3D('',#9004,#7117,#7118);
#5957=AXIS2_PLACEMENT_3D('',#9005,#7119,#7120);
#5958=AXIS2_PLACEMENT_3D('',#9007,#7122,#7123);
#5959=AXIS2_PLACEMENT_3D('',#9011,#7125,#7126);
#5960=AXIS2_PLACEMENT_3D('',#9012,#7127,#7128);
#5961=AXIS2_PLACEMENT_3D('',#9013,#7129,#7130);
#5962=AXIS2_PLACEMENT_3D('',#9014,#7131,#7132);
#5963=AXIS2_PLACEMENT_3D('',#9015,#7133,#7134);
#5964=AXIS2_PLACEMENT_3D('',#9016,#7135,#7136);
#5965=AXIS2_PLACEMENT_3D('',#9017,#7137,#7138);
#5966=AXIS2_PLACEMENT_3D('',#9018,#7139,#7140);
#5967=AXIS2_PLACEMENT_3D('',#9022,#7142,#7143);
#5968=AXIS2_PLACEMENT_3D('',#9027,#7146,#7147);
#5969=AXIS2_PLACEMENT_3D('',#9028,#7148,#7149);
#5970=AXIS2_PLACEMENT_3D('',#9029,#7150,#7151);
#5971=AXIS2_PLACEMENT_3D('',#9030,#7152,#7153);
#5972=AXIS2_PLACEMENT_3D('',#9031,#7154,#7155);
#5973=AXIS2_PLACEMENT_3D('',#9033,#7156,#7157);
#5974=AXIS2_PLACEMENT_3D('',#9035,#7158,#7159);
#5975=AXIS2_PLACEMENT_3D('',#9036,#7160,#7161);
#5976=AXIS2_PLACEMENT_3D('',#9038,#7162,#7163);
#5977=AXIS2_PLACEMENT_3D('',#9040,#7164,#7165);
#5978=AXIS2_PLACEMENT_3D('',#9041,#7166,#7167);
#5979=AXIS2_PLACEMENT_3D('',#9044,#7169,#7170);
#5980=AXIS2_PLACEMENT_3D('',#9047,#7172,#7173);
#5981=AXIS2_PLACEMENT_3D('',#9050,#7175,#7176);
#5982=AXIS2_PLACEMENT_3D('',#9055,#7179,#7180);
#5983=AXIS2_PLACEMENT_3D('',#9056,#7181,#7182);
#5984=AXIS2_PLACEMENT_3D('',#9059,#7184,#7185);
#5985=AXIS2_PLACEMENT_3D('',#9061,#7187,#7188);
#5986=AXIS2_PLACEMENT_3D('',#9063,#7190,#7191);
#5987=AXIS2_PLACEMENT_3D('',#9067,#7193,#7194);
#5988=AXIS2_PLACEMENT_3D('',#9072,#7197,#7198);
#5989=AXIS2_PLACEMENT_3D('',#9075,#7200,#7201);
#5990=AXIS2_PLACEMENT_3D('',#9078,#7203,#7204);
#5991=AXIS2_PLACEMENT_3D('',#9080,#7206,#7207);
#5992=AXIS2_PLACEMENT_3D('',#9081,#7208,#7209);
#5993=AXIS2_PLACEMENT_3D('',#9082,#7210,#7211);
#5994=AXIS2_PLACEMENT_3D('',#9085,#7213,#7214);
#5995=AXIS2_PLACEMENT_3D('',#9087,#7216,#7217);
#5996=AXIS2_PLACEMENT_3D('',#9088,#7218,#7219);
#5997=AXIS2_PLACEMENT_3D('',#9089,#7220,#7221);
#5998=AXIS2_PLACEMENT_3D('',#9090,#7222,#7223);
#5999=AXIS2_PLACEMENT_3D('',#9091,#7224,#7225);
#6000=AXIS2_PLACEMENT_3D('',#9093,#7226,#7227);
#6001=AXIS2_PLACEMENT_3D('',#9095,#7228,#7229);
#6002=AXIS2_PLACEMENT_3D('',#9096,#7230,#7231);
#6505=DIRECTION('',(0.,0.,1.));
#6506=DIRECTION('',(1.,0.,0.));
#7013=DIRECTION('',(-1.,0.,0.));
#7014=DIRECTION('',(0.,0.,1.));
#7015=DIRECTION('',(0.,-1.,0.));
#7016=DIRECTION('',(0.,0.,-1.));
#7017=DIRECTION('',(0.,-1.,0.));
#7018=DIRECTION('',(0.,0.,-1.));
#7019=DIRECTION('',(-1.,0.,0.));
#7020=DIRECTION('',(0.,0.,1.));
#7021=DIRECTION('',(0.,-1.,0.));
#7022=DIRECTION('',(0.,0.,1.));
#7023=DIRECTION('',(0.,-1.,0.));
#7024=DIRECTION('',(0.,0.,-1.));
#7025=DIRECTION('',(0.,0.,-1.));
#7026=DIRECTION('',(0.,0.,-1.));
#7027=DIRECTION('',(-1.,0.,0.));
#7028=DIRECTION('',(1.,0.,0.));
#7029=DIRECTION('',(0.,-1.,0.));
#7030=DIRECTION('',(0.,0.,1.));
#7031=DIRECTION('',(1.,0.,0.));
#7032=DIRECTION('',(-1.,-3.46944695195362E-16,0.));
#7033=DIRECTION('',(0.,0.,1.));
#7034=DIRECTION('',(1.,0.,0.));
#7035=DIRECTION('',(0.,-1.,0.));
#7036=DIRECTION('',(0.,0.,-1.));
#7037=DIRECTION('',(-1.,0.,0.));
#7038=DIRECTION('',(-1.,0.,0.));
#7039=DIRECTION('',(0.,-1.,0.));
#7040=DIRECTION('',(1.,0.,0.));
#7041=DIRECTION('',(1.,0.,0.));
#7042=DIRECTION('',(0.,-1.,0.));
#7043=DIRECTION('',(-1.,0.,0.));
#7044=DIRECTION('',(0.,0.,1.));
#7045=DIRECTION('',(0.,0.,-1.));
#7046=DIRECTION('',(0.,-1.,0.));
#7047=DIRECTION('',(0.,0.,-1.));
#7048=DIRECTION('',(0.,-1.,0.));
#7049=DIRECTION('',(-1.,0.,0.));
#7050=DIRECTION('',(0.,0.,1.));
#7051=DIRECTION('',(0.,0.,1.));
#7052=DIRECTION('',(0.,-1.,0.));
#7053=DIRECTION('',(0.,0.,-1.));
#7054=DIRECTION('',(0.,0.,-1.));
#7055=DIRECTION('',(0.,-1.,0.));
#7056=DIRECTION('',(0.,0.,-1.));
#7057=DIRECTION('',(-1.,0.,0.));
#7058=DIRECTION('',(0.,-1.,0.));
#7059=DIRECTION('',(1.,0.,0.));
#7060=DIRECTION('',(0.,-1.,0.));
#7061=DIRECTION('',(1.,0.,0.));
#7062=DIRECTION('',(0.,0.,-1.));
#7063=DIRECTION('',(-1.,0.,0.));
#7064=DIRECTION('',(0.,-1.,0.));
#7065=DIRECTION('',(-1.,0.,0.));
#7066=DIRECTION('',(0.,-1.,0.));
#7067=DIRECTION('',(1.,0.,0.));
#7068=DIRECTION('',(1.,0.,0.));
#7069=DIRECTION('',(0.,1.,0.));
#7070=DIRECTION('',(0.,0.,1.));
#7071=DIRECTION('',(0.,1.,0.));
#7072=DIRECTION('',(0.,0.,1.));
#7073=DIRECTION('',(0.,-1.,0.));
#7074=DIRECTION('',(0.,0.,-1.));
#7075=DIRECTION('',(0.,-1.,0.));
#7076=DIRECTION('',(0.,1.,0.));
#7077=DIRECTION('',(0.,0.,1.));
#7078=DIRECTION('',(0.,-1.,0.));
#7079=DIRECTION('',(0.,0.,-1.));
#7080=DIRECTION('',(0.,-1.,0.));
#7081=DIRECTION('',(0.,0.,-1.));
#7082=DIRECTION('',(0.,-1.,0.));
#7083=DIRECTION('',(0.,0.,-1.));
#7084=DIRECTION('',(0.,1.,0.));
#7085=DIRECTION('',(0.,0.,1.));
#7086=DIRECTION('',(0.,-1.,0.));
#7087=DIRECTION('',(0.,0.,-1.));
#7088=DIRECTION('',(0.,-1.,0.));
#7089=DIRECTION('',(0.,0.,-1.));
#7090=DIRECTION('',(0.,-1.,0.));
#7091=DIRECTION('',(0.,0.,-1.));
#7092=DIRECTION('',(0.,-1.,0.));
#7093=DIRECTION('',(0.,0.,-1.));
#7094=DIRECTION('',(0.,1.,0.));
#7095=DIRECTION('',(0.,0.,1.));
#7096=DIRECTION('',(0.,1.,0.));
#7097=DIRECTION('',(0.,0.,1.));
#7098=DIRECTION('',(0.,-1.,0.));
#7099=DIRECTION('',(0.,0.,-1.));
#7100=DIRECTION('',(0.,1.,0.));
#7101=DIRECTION('',(0.,0.,1.));
#7102=DIRECTION('',(0.,-1.,0.));
#7103=DIRECTION('',(0.,0.,-1.));
#7104=DIRECTION('',(0.,-1.,0.));
#7105=DIRECTION('',(0.,0.,-1.));
#7106=DIRECTION('',(0.,-1.,0.));
#7107=DIRECTION('',(0.,0.,-1.));
#7108=DIRECTION('',(0.,1.,0.));
#7109=DIRECTION('',(0.,0.,1.));
#7110=DIRECTION('',(0.,-1.,0.));
#7111=DIRECTION('',(0.,-1.,0.));
#7112=DIRECTION('',(0.,0.,-1.));
#7113=DIRECTION('',(0.,-1.,0.));
#7114=DIRECTION('',(0.,0.,-1.));
#7115=DIRECTION('',(0.,-1.,0.));
#7116=DIRECTION('',(0.,0.,-1.));
#7117=DIRECTION('',(0.,-1.,0.));
#7118=DIRECTION('',(0.,0.,-1.));
#7119=DIRECTION('',(0.,0.,-1.));
#7120=DIRECTION('',(-1.,0.,0.));
#7121=DIRECTION('',(1.,0.,0.));
#7122=DIRECTION('',(0.,0.,1.));
#7123=DIRECTION('',(1.,0.,0.));
#7124=DIRECTION('',(1.,-3.46944695195362E-16,0.));
#7125=DIRECTION('',(0.,0.,1.));
#7126=DIRECTION('',(1.,0.,0.));
#7127=DIRECTION('',(0.,-1.,0.));
#7128=DIRECTION('',(0.,0.,-1.));
#7129=DIRECTION('',(0.,-1.,0.));
#7130=DIRECTION('',(0.,0.,-1.));
#7131=DIRECTION('',(0.,-1.,0.));
#7132=DIRECTION('',(0.,0.,-1.));
#7133=DIRECTION('',(0.,-1.,0.));
#7134=DIRECTION('',(0.,0.,-1.));
#7135=DIRECTION('',(0.,-1.,0.));
#7136=DIRECTION('',(0.,0.,-1.));
#7137=DIRECTION('',(0.,-1.,0.));
#7138=DIRECTION('',(0.,0.,-1.));
#7139=DIRECTION('',(0.,1.,0.));
#7140=DIRECTION('',(0.,0.,1.));
#7141=DIRECTION('',(-1.,0.,0.));
#7142=DIRECTION('',(0.,1.,0.));
#7143=DIRECTION('',(0.,0.,1.));
#7144=DIRECTION('',(-1.,0.,0.));
#7145=DIRECTION('',(0.,0.,1.));
#7146=DIRECTION('',(0.,-1.,0.));
#7147=DIRECTION('',(0.,0.,-1.));
#7148=DIRECTION('',(0.,-1.,0.));
#7149=DIRECTION('',(0.,0.,-1.));
#7150=DIRECTION('',(0.,-1.,0.));
#7151=DIRECTION('',(0.,0.,-1.));
#7152=DIRECTION('',(0.,-1.,0.));
#7153=DIRECTION('',(0.,0.,-1.));
#7154=DIRECTION('',(0.,-1.,0.));
#7155=DIRECTION('',(0.,0.,-1.));
#7156=DIRECTION('',(0.,1.,0.));
#7157=DIRECTION('',(0.,0.,1.));
#7158=DIRECTION('',(0.,1.,0.));
#7159=DIRECTION('',(0.,0.,1.));
#7160=DIRECTION('',(0.,1.,0.));
#7161=DIRECTION('',(0.,0.,1.));
#7162=DIRECTION('',(0.,1.,0.));
#7163=DIRECTION('',(0.,0.,1.));
#7164=DIRECTION('',(0.,-1.,0.));
#7165=DIRECTION('',(0.,0.,-1.));
#7166=DIRECTION('',(0.,0.,1.));
#7167=DIRECTION('',(1.,0.,0.));
#7168=DIRECTION('',(0.,0.,1.));
#7169=DIRECTION('',(0.,0.,1.));
#7170=DIRECTION('',(1.,0.,0.));
#7171=DIRECTION('',(0.,0.,1.));
#7172=DIRECTION('',(-3.46944695195362E-16,1.,0.));
#7173=DIRECTION('',(-1.,-3.46944695195362E-16,0.));
#7174=DIRECTION('',(-1.,-3.46944695195362E-16,0.));
#7175=DIRECTION('',(-3.46944695195362E-16,1.,0.));
#7176=DIRECTION('',(-1.,-3.46944695195362E-16,0.));
#7177=DIRECTION('',(-1.,-3.46944695195362E-16,0.));
#7178=DIRECTION('',(0.,0.,1.));
#7179=DIRECTION('',(0.,0.,1.));
#7180=DIRECTION('',(1.,0.,0.));
#7181=DIRECTION('',(0.,0.,1.));
#7182=DIRECTION('',(1.,0.,0.));
#7183=DIRECTION('',(0.,0.,1.));
#7184=DIRECTION('',(-3.46944695195362E-16,-1.,0.));
#7185=DIRECTION('',(1.,-3.46944695195362E-16,0.));
#7186=DIRECTION('',(1.,-3.46944695195362E-16,0.));
#7187=DIRECTION('',(0.,0.,1.));
#7188=DIRECTION('',(1.,0.,0.));
#7189=DIRECTION('',(0.,1.,0.));
#7190=DIRECTION('',(0.,0.,1.));
#7191=DIRECTION('',(1.,0.,0.));
#7192=DIRECTION('',(1.,0.,0.));
#7193=DIRECTION('',(0.,0.,1.));
#7194=DIRECTION('',(1.,0.,0.));
#7195=DIRECTION('',(-1.,0.,0.));
#7196=DIRECTION('',(0.,1.,0.));
#7197=DIRECTION('',(0.,0.,1.));
#7198=DIRECTION('',(1.,0.,0.));
#7199=DIRECTION('',(0.,0.,1.));
#7200=DIRECTION('',(0.,0.,1.));
#7201=DIRECTION('',(1.,0.,0.));
#7202=DIRECTION('',(0.,0.,1.));
#7203=DIRECTION('',(0.,1.,0.));
#7204=DIRECTION('',(0.,0.,1.));
#7205=DIRECTION('',(-1.,0.,0.));
#7206=DIRECTION('',(0.,1.,0.));
#7207=DIRECTION('',(0.,0.,1.));
#7208=DIRECTION('',(0.,0.,1.));
#7209=DIRECTION('',(1.,0.,0.));
#7210=DIRECTION('',(0.,0.,1.));
#7211=DIRECTION('',(1.,0.,0.));
#7212=DIRECTION('',(0.,0.,1.));
#7213=DIRECTION('',(0.,-1.,0.));
#7214=DIRECTION('',(0.,0.,-1.));
#7215=DIRECTION('',(1.,0.,0.));
#7216=DIRECTION('',(0.,0.,1.));
#7217=DIRECTION('',(1.,0.,0.));
#7218=DIRECTION('',(0.,1.,0.));
#7219=DIRECTION('',(0.,0.,1.));
#7220=DIRECTION('',(0.,-1.,0.));
#7221=DIRECTION('',(0.,0.,-1.));
#7222=DIRECTION('',(0.,1.,0.));
#7223=DIRECTION('',(0.,0.,1.));
#7224=DIRECTION('',(0.,1.,0.));
#7225=DIRECTION('',(0.,0.,1.));
#7226=DIRECTION('',(0.,1.,0.));
#7227=DIRECTION('',(0.,0.,1.));
#7228=DIRECTION('',(0.,1.,0.));
#7229=DIRECTION('',(0.,0.,1.));
#7230=DIRECTION('',(0.,-1.,0.));
#7231=DIRECTION('',(0.,0.,-1.));
#8391=CARTESIAN_POINT('',(0.,0.,0.));
#8881=CARTESIAN_POINT('',(-0.006,0.025,0.006));
#8882=CARTESIAN_POINT('',(-0.006,0.025,0.004));
#8883=CARTESIAN_POINT('',(-0.006,0.,0.004));
#8884=CARTESIAN_POINT('',(-0.006,0.0184403410758551,0.004));
#8885=CARTESIAN_POINT('',(-0.006,0.0184403410758551,0.006));
#8886=CARTESIAN_POINT('',(-0.006,0.0184403410758551,-0.004));
#8887=CARTESIAN_POINT('',(-0.006,0.025,-0.004));
#8888=CARTESIAN_POINT('',(-0.006,0.,-0.004));
#8889=CARTESIAN_POINT('',(-0.006,0.,0.006));
#8890=CARTESIAN_POINT('',(-0.006,0.025,0.006));
#8891=CARTESIAN_POINT('',(-0.006,0.025,-0.004));
#8892=CARTESIAN_POINT('',(-0.006,0.025,-0.004));
#8893=CARTESIAN_POINT('',(-0.006,0.0215596589241449,-0.004));
#8894=CARTESIAN_POINT('',(-0.006,0.0215596589241449,0.006));
#8895=CARTESIAN_POINT('',(-0.006,0.0215596589241449,0.004));
#8896=CARTESIAN_POINT('',(-0.006,0.025,0.004));
#8897=CARTESIAN_POINT('',(-0.006,0.025,0.004));
#8898=CARTESIAN_POINT('',(-0.006,0.025,0.006));
#8899=CARTESIAN_POINT('',(-0.006,0.025,0.));
#8900=CARTESIAN_POINT('',(-0.006,0.025,0.006));
#8901=CARTESIAN_POINT('',(-0.006,0.025,0.006));
#8902=CARTESIAN_POINT('',(-0.006,0.0184403410758551,0.006));
#8903=CARTESIAN_POINT('',(-0.004,0.0184403410758551,0.006));
#8904=CARTESIAN_POINT('',(0.004,0.0184403410758551,0.006));
#8905=CARTESIAN_POINT('',(-0.004,0.,0.006));
#8906=CARTESIAN_POINT('',(-0.004,0.0104638876866717,0.006));
#8907=CARTESIAN_POINT('',(-0.0025,0.00914101203113945,0.006));
#8908=CARTESIAN_POINT('',(-0.0025,0.0111410120311394,0.006));
#8909=CARTESIAN_POINT('',(-0.0025,0.0111410120311394,0.006));
#8910=CARTESIAN_POINT('',(0.0025,0.0111410120311394,0.006));
#8911=CARTESIAN_POINT('',(0.0025,0.00914101203113945,0.006));
#8912=CARTESIAN_POINT('',(0.004,0.0104638876866717,0.006));
#8913=CARTESIAN_POINT('',(0.004,0.025,0.006));
#8914=CARTESIAN_POINT('',(-0.006,0.025,0.006));
#8915=CARTESIAN_POINT('',(-0.006,0.0215596589241449,0.006));
#8916=CARTESIAN_POINT('',(0.004,0.0215596589241449,0.006));
#8917=CARTESIAN_POINT('',(-0.004,0.0215596589241449,0.006));
#8918=CARTESIAN_POINT('',(0.004,0.025,0.006));
#8919=CARTESIAN_POINT('',(0.004,0.025,0.006));
#8920=CARTESIAN_POINT('',(-0.006,0.025,0.006));
#8921=CARTESIAN_POINT('',(0.,0.025,0.006));
#8922=CARTESIAN_POINT('',(-0.006,0.025,0.006));
#8923=CARTESIAN_POINT('',(-0.004,0.025,0.006));
#8924=CARTESIAN_POINT('',(-0.004,0.,0.006));
#8925=CARTESIAN_POINT('',(0.006,0.025,0.006));
#8926=CARTESIAN_POINT('',(0.006,0.0184403410758551,0.006));
#8927=CARTESIAN_POINT('',(0.006,0.0184403410758551,0.004));
#8928=CARTESIAN_POINT('',(0.006,0.0184403410758551,-0.004));
#8929=CARTESIAN_POINT('',(0.006,0.025,0.004));
#8930=CARTESIAN_POINT('',(0.006,0.,0.004));
#8931=CARTESIAN_POINT('',(0.006,0.,0.006));
#8932=CARTESIAN_POINT('',(0.006,0.,-0.004));
#8933=CARTESIAN_POINT('',(0.006,0.025,-0.004));
#8934=CARTESIAN_POINT('',(0.006,0.025,0.006));
#8935=CARTESIAN_POINT('',(0.006,0.0215596589241449,0.006));
#8936=CARTESIAN_POINT('',(0.006,0.0215596589241449,-0.004));
#8937=CARTESIAN_POINT('',(0.006,0.0215596589241449,0.004));
#8938=CARTESIAN_POINT('',(0.006,0.025,-0.004));
#8939=CARTESIAN_POINT('',(0.006,0.025,-0.004));
#8940=CARTESIAN_POINT('',(0.006,0.025,0.006));
#8941=CARTESIAN_POINT('',(0.006,0.025,0.));
#8942=CARTESIAN_POINT('',(0.006,0.025,0.006));
#8943=CARTESIAN_POINT('',(0.006,0.025,0.004));
#8944=CARTESIAN_POINT('',(0.006,0.025,0.004));
#8945=CARTESIAN_POINT('',(-0.006,0.025,-0.006));
#8946=CARTESIAN_POINT('',(-0.004,0.025,-0.006));
#8947=CARTESIAN_POINT('',(-0.004,0.,-0.006));
#8948=CARTESIAN_POINT('',(-0.004,0.0184403410758551,-0.006));
#8949=CARTESIAN_POINT('',(-0.006,0.0184403410758551,-0.006));
#8950=CARTESIAN_POINT('',(0.004,0.0184403410758551,-0.006));
#8951=CARTESIAN_POINT('',(0.004,0.,-0.006));
#8952=CARTESIAN_POINT('',(0.004,0.,-0.006));
#8953=CARTESIAN_POINT('',(-0.006,0.,-0.006));
#8954=CARTESIAN_POINT('',(-0.006,0.025,-0.006));
#8955=CARTESIAN_POINT('',(0.004,0.,-0.006));
#8956=CARTESIAN_POINT('',(0.004,0.025,-0.006));
#8957=CARTESIAN_POINT('',(0.004,0.0215596589241449,-0.006));
#8958=CARTESIAN_POINT('',(-0.006,0.0215596589241449,-0.006));
#8959=CARTESIAN_POINT('',(-0.004,0.0215596589241449,-0.006));
#8960=CARTESIAN_POINT('',(-0.004,0.025,-0.006));
#8961=CARTESIAN_POINT('',(-0.004,0.025,-0.006));
#8962=CARTESIAN_POINT('',(-0.006,0.025,-0.006));
#8963=CARTESIAN_POINT('',(0.,0.025,-0.006));
#8964=CARTESIAN_POINT('',(-0.006,0.025,-0.006));
#8965=CARTESIAN_POINT('',(-0.004,0.025,0.004));
#8966=CARTESIAN_POINT('',(-0.004,0.0184403410758551,0.004));
#8967=CARTESIAN_POINT('',(-0.004,0.,0.004));
#8968=CARTESIAN_POINT('',(-0.004,0.,0.006));
#8969=CARTESIAN_POINT('',(-0.004,0.,0.006));
#8970=CARTESIAN_POINT('',(-0.004,0.00781813637560716,0.006));
#8971=CARTESIAN_POINT('',(-0.004,0.0104638876866717,0.006));
#8972=CARTESIAN_POINT('',(-0.00432213201520761,0.0100986243145697,0.006));
#8973=CARTESIAN_POINT('',(-0.00467795026178238,0.00914209250915622,0.00587298337765155));
#8974=CARTESIAN_POINT('',(-0.00432196721766239,0.0081832128848572,0.006));
#8975=CARTESIAN_POINT('',(-0.004,0.00781813637560716,0.006));
#8976=CARTESIAN_POINT('',(-0.004,0.025,0.004));
#8977=CARTESIAN_POINT('',(-0.004,0.0215596589241449,0.004));
#8978=CARTESIAN_POINT('',(-0.004,0.025,0.004));
#8979=CARTESIAN_POINT('',(-0.004,0.025,-0.004));
#8980=CARTESIAN_POINT('',(-0.004,0.0184403410758551,-0.004));
#8981=CARTESIAN_POINT('',(-0.004,0.,-0.004));
#8982=CARTESIAN_POINT('',(-0.004,0.025,-0.004));
#8983=CARTESIAN_POINT('',(-0.004,0.0215596589241449,-0.004));
#8984=CARTESIAN_POINT('',(-0.004,0.025,-0.004));
#8985=CARTESIAN_POINT('',(0.004,0.025,-0.004));
#8986=CARTESIAN_POINT('',(0.004,0.0184403410758551,-0.004));
#8987=CARTESIAN_POINT('',(0.004,0.,-0.004));
#8988=CARTESIAN_POINT('',(0.004,0.025,-0.004));
#8989=CARTESIAN_POINT('',(0.004,0.0215596589241449,-0.004));
#8990=CARTESIAN_POINT('',(0.004,0.025,-0.004));
#8991=CARTESIAN_POINT('',(0.004,0.025,0.004));
#8992=CARTESIAN_POINT('',(0.004,0.0184403410758551,0.004));
#8993=CARTESIAN_POINT('',(0.004,0.00781813637560717,0.006));
#8994=CARTESIAN_POINT('',(0.00432213201520761,0.0081833997477092,0.006));
#8995=CARTESIAN_POINT('',(0.00467795026178238,0.00913993155312269,0.00587298337765155));
#8996=CARTESIAN_POINT('',(0.00432196721766239,0.0100988111774217,0.006));
#8997=CARTESIAN_POINT('',(0.004,0.0104638876866717,0.006));
#8998=CARTESIAN_POINT('',(0.004,0.00781813637560717,0.006));
#8999=CARTESIAN_POINT('',(0.004,0.025,0.006));
#9000=CARTESIAN_POINT('',(0.004,0.,0.006));
#9001=CARTESIAN_POINT('',(0.004,0.,0.004));
#9002=CARTESIAN_POINT('',(0.004,0.025,0.004));
#9003=CARTESIAN_POINT('',(0.004,0.0215596589241449,0.004));
#9004=CARTESIAN_POINT('',(0.004,0.025,0.004));
#9005=CARTESIAN_POINT('',(-0.006,0.025,0.006));
#9006=CARTESIAN_POINT('',(-0.006,0.,0.006));
#9007=CARTESIAN_POINT('',(0.0025,0.00914101203113945,0.006));
#9008=CARTESIAN_POINT('',(0.0025,0.00714101203113945,0.006));
#9009=CARTESIAN_POINT('',(-0.0025,0.00714101203113946,0.006));
#9010=CARTESIAN_POINT('',(-0.0025,0.00714101203113946,0.006));
#9011=CARTESIAN_POINT('',(-0.0025,0.00914101203113945,0.006));
#9012=CARTESIAN_POINT('',(0.,0.025,0.));
#9013=CARTESIAN_POINT('',(0.,0.025,0.));
#9014=CARTESIAN_POINT('',(0.,0.025,0.));
#9015=CARTESIAN_POINT('',(0.,0.025,0.));
#9016=CARTESIAN_POINT('',(0.,0.025,0.));
#9017=CARTESIAN_POINT('',(0.,0.025,0.));
#9018=CARTESIAN_POINT('',(0.0025,0.0106410120311394,-0.0015));
#9019=CARTESIAN_POINT('',(0.0025,0.0106410120311394,0.001));
#9020=CARTESIAN_POINT('',(0.0025,0.0106410120311394,0.001));
#9021=CARTESIAN_POINT('',(0.00111803398874989,0.0106410120311394,0.001));
#9022=CARTESIAN_POINT('',(0.,0.0106410120311394,0.));
#9023=CARTESIAN_POINT('',(0.,0.0106410120311394,-0.0015));
#9024=CARTESIAN_POINT('',(0.0025,0.0106410120311394,-0.0015));
#9025=CARTESIAN_POINT('',(0.0025,0.0106410120311394,-0.0015));
#9026=CARTESIAN_POINT('',(0.0025,0.0106410120311394,-0.0015));
#9027=CARTESIAN_POINT('',(0.,0.025,0.));
#9028=CARTESIAN_POINT('',(0.,0.025,0.));
#9029=CARTESIAN_POINT('',(0.,0.,0.));
#9030=CARTESIAN_POINT('',(0.,0.038,0.));
#9031=CARTESIAN_POINT('',(0.,0.027,0.));
#9032=CARTESIAN_POINT('',(0.,0.027,-0.004));
#9033=CARTESIAN_POINT('',(0.,0.0365,0.));
#9034=CARTESIAN_POINT('',(0.,0.0365,0.004));
#9035=CARTESIAN_POINT('',(0.,0.038,0.));
#9036=CARTESIAN_POINT('',(0.,0.038,0.));
#9037=CARTESIAN_POINT('',(0.,0.038,0.0015));
#9038=CARTESIAN_POINT('',(0.,0.038,0.));
#9039=CARTESIAN_POINT('',(0.,0.038,0.0025));
#9040=CARTESIAN_POINT('',(0.,0.038,0.));
#9041=CARTESIAN_POINT('',(-0.0025,0.00914101203113945,0.001));
#9042=CARTESIAN_POINT('',(-0.0025,0.00714101203113946,0.001));
#9043=CARTESIAN_POINT('',(-0.0025,0.00714101203113946,0.001));
#9044=CARTESIAN_POINT('',(-0.0025,0.00914101203113945,0.001));
#9045=CARTESIAN_POINT('',(-0.0025,0.0111410120311394,0.001));
#9046=CARTESIAN_POINT('',(-0.0025,0.0111410120311394,0.001));
#9047=CARTESIAN_POINT('',(-0.0025,0.0111410120311394,0.001));
#9048=CARTESIAN_POINT('',(-0.0025,0.0111410120311394,0.001));
#9049=CARTESIAN_POINT('',(-0.00111803398874989,0.0111410120311394,0.001));
#9050=CARTESIAN_POINT('',(0.,0.0111410120311394,0.));
#9051=CARTESIAN_POINT('',(0.00111803398874989,0.0111410120311394,0.001));
#9052=CARTESIAN_POINT('',(-0.0025,0.0111410120311394,0.001));
#9053=CARTESIAN_POINT('',(0.0025,0.0111410120311394,0.001));
#9054=CARTESIAN_POINT('',(0.0025,0.0111410120311394,0.001));
#9055=CARTESIAN_POINT('',(0.0025,0.00914101203113945,0.001));
#9056=CARTESIAN_POINT('',(0.0025,0.00914101203113945,0.001));
#9057=CARTESIAN_POINT('',(0.0025,0.00714101203113945,0.001));
#9058=CARTESIAN_POINT('',(0.0025,0.00714101203113945,0.001));
#9059=CARTESIAN_POINT('',(-0.0025,0.00714101203113946,0.001));
#9060=CARTESIAN_POINT('',(-0.0025,0.00714101203113946,0.001));
#9061=CARTESIAN_POINT('',(-0.0025,0.00914101203113945,0.001));
#9062=CARTESIAN_POINT('',(0.00111803398874989,0.00639837134402017,0.001));
#9063=CARTESIAN_POINT('',(0.0025,0.00914101203113945,0.001));
#9064=CARTESIAN_POINT('',(0.0025,0.00764101203113946,0.001));
#9065=CARTESIAN_POINT('',(-0.0025,0.00764101203113946,0.001));
#9066=CARTESIAN_POINT('',(-0.0025,0.00764101203113946,0.001));
#9067=CARTESIAN_POINT('',(-0.0025,0.00914101203113945,0.001));
#9068=CARTESIAN_POINT('',(-0.0025,0.0106410120311394,0.001));
#9069=CARTESIAN_POINT('',(0.0025,0.0106410120311394,0.001));
#9070=CARTESIAN_POINT('',(-0.00111803398874989,0.0106410120311394,0.001));
#9071=CARTESIAN_POINT('',(-0.00111803398874989,0.00639837134402017,0.001));
#9072=CARTESIAN_POINT('',(-0.0025,0.00914101203113945,-0.0015));
#9073=CARTESIAN_POINT('',(-0.0025,0.00764101203113946,-0.0015));
#9074=CARTESIAN_POINT('',(-0.0025,0.00764101203113946,-0.0015));
#9075=CARTESIAN_POINT('',(-0.0025,0.00914101203113945,-0.0015));
#9076=CARTESIAN_POINT('',(-0.0025,0.0106410120311394,-0.0015));
#9077=CARTESIAN_POINT('',(-0.0025,0.0106410120311394,-0.0015));
#9078=CARTESIAN_POINT('',(0.0025,0.0106410120311394,-0.0015));
#9079=CARTESIAN_POINT('',(0.0025,0.0106410120311394,-0.0015));
#9080=CARTESIAN_POINT('',(0.,0.0106410120311394,0.));
#9081=CARTESIAN_POINT('',(0.0025,0.00914101203113945,-0.0015));
#9082=CARTESIAN_POINT('',(0.0025,0.00914101203113945,-0.0015));
#9083=CARTESIAN_POINT('',(0.0025,0.00764101203113946,-0.0015));
#9084=CARTESIAN_POINT('',(0.0025,0.00764101203113946,-0.0015));
#9085=CARTESIAN_POINT('',(-0.0025,0.00764101203113946,-0.0015));
#9086=CARTESIAN_POINT('',(-0.0025,0.00764101203113946,-0.0015));
#9087=CARTESIAN_POINT('',(-0.0025,0.00914101203113945,-0.0015));
#9088=CARTESIAN_POINT('',(0.,0.00639837134402017,0.));
#9089=CARTESIAN_POINT('',(0.,0.027,0.));
#9090=CARTESIAN_POINT('',(0.,0.0359035031847133,0.));
#9091=CARTESIAN_POINT('',(0.,0.0184403410758551,0.));
#9092=CARTESIAN_POINT('',(0.,0.0184403410758551,0.00500637669063053));
#9093=CARTESIAN_POINT('',(0.,0.0215596589241449,0.));
#9094=CARTESIAN_POINT('',(0.,0.0215596589241449,0.00500637669063053));
#9095=CARTESIAN_POINT('',(0.00803591354510047,0.0184403410758551,0.));
#9096=CARTESIAN_POINT('',(0.00803591354510047,0.0215596589241449,0.));
#10141=MECHANICAL_DESIGN_GEOMETRIC_PRESENTATION_REPRESENTATION('',(#5556),#10142);
#10142=(
GEOMETRIC_REPRESENTATION_CONTEXT(3)
GLOBAL_UNCERTAINTY_ASSIGNED_CONTEXT((#10158))
GLOBAL_UNIT_ASSIGNED_CONTEXT((#10176,#10175,#10174))
REPRESENTATION_CONTEXT('MAS-674','TOP_LEVEL_ASSEMBLY_PART')
);
#10146=(
GEOMETRIC_REPRESENTATION_CONTEXT(3)
GLOBAL_UNCERTAINTY_ASSIGNED_CONTEXT((#10162))
GLOBAL_UNIT_ASSIGNED_CONTEXT((#10176,#10175,#10174))
REPRESENTATION_CONTEXT('Part 1','COMPONENT_PART')
);
#10158=UNCERTAINTY_MEASURE_WITH_UNIT(LENGTH_MEASURE(1.E-8),#10176,
'DISTANCE_ACCURACY_VALUE','Maximum Tolerance applied to model');
#10162=UNCERTAINTY_MEASURE_WITH_UNIT(LENGTH_MEASURE(2.E-5),#10176,
'DISTANCE_ACCURACY_VALUE','Maximum Tolerance applied to model');
#10174=(
NAMED_UNIT(*)
SI_UNIT($,.STERADIAN.)
SOLID_ANGLE_UNIT()
);
#10175=(
NAMED_UNIT(*)
PLANE_ANGLE_UNIT()
SI_UNIT($,.RADIAN.)
);
#10176=(
LENGTH_UNIT()
NAMED_UNIT(*)
SI_UNIT($,.METRE.)
);
#10186=PRODUCT_DEFINITION_SHAPE('','',#10214);
#10214=PRODUCT_DEFINITION('','',#10246,#10230);
#10230=PRODUCT_DEFINITION_CONTEXT('',#10323,'design');
#10246=PRODUCT_DEFINITION_FORMATION_WITH_SPECIFIED_SOURCE('','',#10278,
 .NOT_KNOWN.);
#10278=PRODUCT('Part 1','Part 1','Part 1',(#10310));
#10310=PRODUCT_CONTEXT('',#10323,'mechanical');
#10323=APPLICATION_CONTEXT('managed model based 3d engineering');
ENDSEC;
END-ISO-10303-21;
